ISO-10303-21;
HEADER;
FILE_DESCRIPTION (('STEP AP214'),
    '1' );
FILE_NAME ('plain washer 10669 type nl_iso_ISO 10669-5.4-N.step',
    '2026-10-27T17:01:19',
    ( '' ),
    ( '' ),
    'SwSTEP 2.0',
    'SolidWorks 2026',
    '' );
FILE_SCHEMA (( 'AUTOMOTIVE_DESIGN' ));
ENDSEC;

DATA;
#13=( GEOMETRIC_REPRESENTATION_CONTEXT ( 3 ) GLOBAL_UNCERTAINTY_ASSIGNED_CONTEXT ( ( #9752 ) ) GLOBAL_UNIT_ASSIGNED_CONTEXT ( ( #1212, #12871, #12805 ) ) REPRESENTATION_CONTEXT ( 'NONE', 'WORKASPACE' ) );
#29=AXIS2_PLACEMENT_3D ( 'NONE', #668, #3321, #5190 ) ;
#46=ORIENTED_EDGE ( 'NONE', *, *, #6815, .F. ) ;
#52=ADVANCED_FACE ( 'NONE', ( #11739, #7114 ), #5117, .T. ) ;
#97=ORIENTED_EDGE ( 'NONE', *, *, #10462, .F. ) ;
#124=PRODUCT ( 'plain washer 10669 type nl_iso_ISO 10669-5.4-N', 'plain washer 10669 type nl_iso_ISO 10669-5.4-N', '', ( #6717 ) ) ;
#232=SURFACE_SIDE_STYLE ('',( #9558 ) ) ;
#238=VERTEX_POINT ( 'NONE', #752 ) ;
#275=CARTESIAN_POINT ( 'NONE',  ( 0.000000000000000000, 0.000000000000000000, 0.000000000000000000 ) ) ;
#369=DIRECTION ( 'NONE',  ( 0.000000000000000000, 0.000000000000000000, -1.000000000000000000 ) ) ;
#392=EDGE_CURVE ( 'NONE', #3159, #7275, #4422, .T. ) ;
#421=AXIS2_PLACEMENT_3D ( 'NONE', #6054, #10559, #10487 ) ;
#584=DIRECTION ( 'NONE',  ( 1.000000000000000000, 0.000000000000000000, 0.000000000000000000 ) ) ;
#668=CARTESIAN_POINT ( 'NONE',  ( 0.000000000000000000, 0.000000000000000000, 0.000000000000000000 ) ) ;
#752=CARTESIAN_POINT ( 'NONE',  ( 1.600000000000000089, 8.572527594031473190E-16, -7.000000000000000000 ) ) ;
#877=ORIENTED_EDGE ( 'NONE', *, *, #6737, .T. ) ;
#889=DIRECTION ( 'NONE',  ( -1.000000000000000000, -0.000000000000000000, -0.000000000000000000 ) ) ;
#912=EDGE_LOOP ( 'NONE', ( #2980, #14447 ) ) ;
#960=AXIS2_PLACEMENT_3D ( 'NONE', #6772, #7955, #7892 ) ;
#961=CIRCLE ( 'NONE', #6624, 2.700000000000000178 ) ;
#1078=VERTEX_POINT ( 'NONE', #7372 ) ;
#1210=DIRECTION ( 'NONE',  ( -1.000000000000000000, -0.000000000000000000, -0.000000000000000000 ) ) ;
#1212=( LENGTH_UNIT ( ) NAMED_UNIT ( * ) SI_UNIT ( .MILLI., .METRE. ) );
#1325=CYLINDRICAL_SURFACE ( 'NONE', #5457, 2.700000000000000178 ) ;
#1480=DIRECTION ( 'NONE',  ( 1.000000000000000000, 0.000000000000000000, 0.000000000000000000 ) ) ;
#1488=ORIENTED_EDGE ( 'NONE', *, *, #5661, .F. ) ;
#1785=DIRECTION ( 'NONE',  ( 0.000000000000000000, 0.000000000000000000, -1.000000000000000000 ) ) ;
#1788=ADVANCED_FACE ( 'NONE', ( #2810 ), #13888, .T. ) ;
#1900=CIRCLE ( 'NONE', #10153, 7.000000000000000000 ) ;
#1937=UNCERTAINTY_MEASURE_WITH_UNIT (LENGTH_MEASURE( 1.000000000000000082E-05 ), #10196, 'distance_accuracy_value', 'NONE');
#1973=EDGE_LOOP ( 'NONE', ( #5043, #10935, #6632, #46 ) ) ;
#2030=CARTESIAN_POINT ( 'NONE',  ( 1.600000000000000089, 3.306546357697853733E-16, -2.700000000000000178 ) ) ;
#2255=CARTESIAN_POINT ( 'NONE',  ( 1.600000000000000089, 0.000000000000000000, 2.700000000000000178 ) ) ;
#2529=MANIFOLD_SOLID_BREP ( 'Base-Extrude', #14002 ) ;
#2533=APPLICATION_CONTEXT ( 'automotive_design' ) ;
#2536=ORIENTED_EDGE ( 'NONE', *, *, #4940, .F. ) ;
#2588=ADVANCED_FACE ( 'NONE', ( #13581 ), #7905, .F. ) ;
#2707=CARTESIAN_POINT ( 'NONE',  ( 1.600000000000000089, 0.000000000000000000, 0.000000000000000000 ) ) ;
#2752=PRESENTATION_STYLE_ASSIGNMENT (( #4775 ) ) ;
#2784=EDGE_LOOP ( 'NONE', ( #4869, #11981, #9283, #7174 ) ) ;
#2810=FACE_OUTER_BOUND ( 'NONE', #2784, .T. ) ;
#2831=CARTESIAN_POINT ( 'NONE',  ( 1.600000000000000089, 0.000000000000000000, 2.700000000000000178 ) ) ;
#2880=VERTEX_POINT ( 'NONE', #6706 ) ;
#2887=CIRCLE ( 'NONE', #29, 7.000000000000000000 ) ;
#2980=ORIENTED_EDGE ( 'NONE', *, *, #10462, .T. ) ;
#3019=ADVANCED_FACE ( 'NONE', ( #3532 ), #7061, .T. ) ;
#3159=VERTEX_POINT ( 'NONE', #10052 ) ;
#3247=STYLED_ITEM('',(#14681),#2529);
#3321=DIRECTION ( 'NONE',  ( 1.000000000000000000, 0.000000000000000000, 0.000000000000000000 ) ) ;
#3343=PRODUCT_DEFINITION_SHAPE ( 'NONE', 'NONE',  #9297 ) ;
#3392=SHAPE_REPRESENTATION ( 'plain washer 10669 type nl_iso_ISO 10669-5.4-N', ( #9440 ), #13 ) ;
#3532=FACE_OUTER_BOUND ( 'NONE', #7190, .T. ) ;
#3552=CARTESIAN_POINT ( 'NONE',  ( 1.600000000000000089, 0.000000000000000000, 0.000000000000000000 ) ) ;
#3560=AXIS2_PLACEMENT_3D ( 'NONE', #7173, #584, #5393 ) ;
#3694=ORIENTED_EDGE ( 'NONE', *, *, #8562, .T. ) ;
#3769=EDGE_LOOP ( 'NONE', ( #13617, #2536 ) ) ;
#3875=EDGE_LOOP ( 'NONE', ( #9687, #10191 ) ) ;
#3963=DIRECTION ( 'NONE',  ( 1.000000000000000000, 0.000000000000000000, 0.000000000000000000 ) ) ;
#4043=DIRECTION ( 'NONE',  ( 0.000000000000000000, 0.000000000000000000, -1.000000000000000000 ) ) ;
#4156=VERTEX_POINT ( 'NONE', #4642 ) ;
#4262=ORIENTED_EDGE ( 'NONE', *, *, #6737, .F. ) ;
#4347=CARTESIAN_POINT ( 'NONE',  ( 0.000000000000000000, 0.000000000000000000, 0.000000000000000000 ) ) ;
#4392=CARTESIAN_POINT ( 'NONE',  ( 1.600000000000000089, 8.572527594031473190E-16, -7.000000000000000000 ) ) ;
#4420=AXIS2_PLACEMENT_3D ( 'NONE', #11536, #10441, #369 ) ;
#4422=CIRCLE ( 'NONE', #11953, 2.700000000000000178 ) ;
#4430=( GEOMETRIC_REPRESENTATION_CONTEXT ( 3 ) GLOBAL_UNCERTAINTY_ASSIGNED_CONTEXT ( ( #1937 ) ) GLOBAL_UNIT_ASSIGNED_CONTEXT ( ( #10196, #14542, #13437 ) ) REPRESENTATION_CONTEXT ( 'NONE', 'WORKASPACE' ) );
#4642=CARTESIAN_POINT ( 'NONE',  ( 0.000000000000000000, 0.000000000000000000, 7.000000000000000000 ) ) ;
#4680=AXIS2_PLACEMENT_3D ( 'NONE', #3552, #9235, #10414 ) ;
#4775=SURFACE_STYLE_USAGE ( .BOTH. , #232 ) ;
#4813=EDGE_LOOP ( 'NONE', ( #3694, #877 ) ) ;
#4814=DIRECTION ( 'NONE',  ( 0.000000000000000000, 0.000000000000000000, -1.000000000000000000 ) ) ;
#4869=ORIENTED_EDGE ( 'NONE', *, *, #4923, .F. ) ;
#4893=FACE_OUTER_BOUND ( 'NONE', #3769, .T. ) ;
#4901=ORIENTED_EDGE ( 'NONE', *, *, #6531, .F. ) ;
#4923=EDGE_CURVE ( 'NONE', #238, #2880, #4980, .T. ) ;
#4940=EDGE_CURVE ( 'NONE', #11405, #4156, #1900, .T. ) ;
#4980=CIRCLE ( 'NONE', #7092, 7.000000000000000000 ) ;
#5043=ORIENTED_EDGE ( 'NONE', *, *, #7396, .T. ) ;
#5117=PLANE ( 'NONE',  #6677 ) ;
#5190=DIRECTION ( 'NONE',  ( 0.000000000000000000, 0.000000000000000000, -1.000000000000000000 ) ) ;
#5358=ORIENTED_EDGE ( 'NONE', *, *, #11410, .T. ) ;
#5393=DIRECTION ( 'NONE',  ( 0.000000000000000000, 0.000000000000000000, -1.000000000000000000 ) ) ;
#5408=AXIS2_PLACEMENT_3D ( 'NONE', #2707, #3963, #4043 ) ;
#5455=CIRCLE ( 'NONE', #960, 7.000000000000000000 ) ;
#5457=AXIS2_PLACEMENT_3D ( 'NONE', #7158, #6937, #11713 ) ;
#5515=ORIENTED_EDGE ( 'NONE', *, *, #392, .T. ) ;
#5661=EDGE_CURVE ( 'NONE', #3159, #1078, #12146, .T. ) ;
#5806=DIRECTION ( 'NONE',  ( 0.000000000000000000, 0.000000000000000000, 1.000000000000000000 ) ) ;
#5833=MECHANICAL_DESIGN_GEOMETRIC_PRESENTATION_REPRESENTATION('',(#3247),#4430);
#5932=COLOUR_RGB ( '',1.000000000000000000, 0.9490196078431372140, 0.9098039215686274384 ) ;
#5941=( NAMED_UNIT ( * ) PLANE_ANGLE_UNIT ( ) SI_UNIT ( $, .RADIAN. ) );
#6054=CARTESIAN_POINT ( 'NONE',  ( 1.600000000000000089, 0.000000000000000000, 0.000000000000000000 ) ) ;
#6225=DIRECTION ( 'NONE',  ( 1.000000000000000000, 0.000000000000000000, 0.000000000000000000 ) ) ;
#6226=CARTESIAN_POINT ( 'NONE',  ( 0.000000000000000000, 8.572527594031473190E-16, -7.000000000000000000 ) ) ;
#6288=CARTESIAN_POINT ( 'NONE',  ( 1.600000000000000089, 0.000000000000000000, 0.000000000000000000 ) ) ;
#6343=VECTOR ( 'NONE', #889, 1000.000000000000000 ) ;
#6389=CARTESIAN_POINT ( 'NONE',  ( 1.600000000000000089, 0.000000000000000000, 0.000000000000000000 ) ) ;
#6417=DIRECTION ( 'NONE',  ( 1.000000000000000000, 0.000000000000000000, 0.000000000000000000 ) ) ;
#6531=EDGE_CURVE ( 'NONE', #238, #11405, #8074, .T. ) ;
#6624=AXIS2_PLACEMENT_3D ( 'NONE', #275, #1480, #4814 ) ;
#6632=ORIENTED_EDGE ( 'NONE', *, *, #8562, .F. ) ;
#6640=STYLED_ITEM ( 'NONE', ( #2752 ), #7736 ) ;
#6661=PRODUCT_DEFINITION_FORMATION_WITH_SPECIFIED_SOURCE ( 'ANY', '', #124, .NOT_KNOWN. ) ;
#6677=AXIS2_PLACEMENT_3D ( 'NONE', #6288, #6225, #1785 ) ;
#6678=DIRECTION ( 'NONE',  ( 1.000000000000000000, 0.000000000000000000, 0.000000000000000000 ) ) ;
#6706=CARTESIAN_POINT ( 'NONE',  ( 1.600000000000000089, 0.000000000000000000, 7.000000000000000000 ) ) ;
#6717=PRODUCT_CONTEXT ( 'NONE', #2533, 'mechanical' ) ;
#6737=EDGE_CURVE ( 'NONE', #1078, #13362, #12672, .T. ) ;
#6772=CARTESIAN_POINT ( 'NONE',  ( 1.600000000000000089, 0.000000000000000000, 0.000000000000000000 ) ) ;
#6815=EDGE_CURVE ( 'NONE', #7275, #13362, #14272, .T. ) ;
#6921=CARTESIAN_POINT ( 'NONE',  ( 1.600000000000000089, 0.000000000000000000, 0.000000000000000000 ) ) ;
#6937=DIRECTION ( 'NONE',  ( -1.000000000000000000, -0.000000000000000000, -0.000000000000000000 ) ) ;
#7061=CYLINDRICAL_SURFACE ( 'NONE', #13883, 7.000000000000000000 ) ;
#7092=AXIS2_PLACEMENT_3D ( 'NONE', #6389, #6678, #13313 ) ;
#7114=FACE_BOUND ( 'NONE', #3875, .T. ) ;
#7158=CARTESIAN_POINT ( 'NONE',  ( 1.600000000000000089, 0.000000000000000000, 0.000000000000000000 ) ) ;
#7173=CARTESIAN_POINT ( 'NONE',  ( 0.000000000000000000, 0.000000000000000000, 0.000000000000000000 ) ) ;
#7174=ORIENTED_EDGE ( 'NONE', *, *, #7699, .F. ) ;
#7189=FILL_AREA_STYLE ('',( #10581 ) ) ;
#7190=EDGE_LOOP ( 'NONE', ( #4901, #97, #9526, #5358 ) ) ;
#7275=VERTEX_POINT ( 'NONE', #2255 ) ;
#7349=APPLICATION_CONTEXT ( 'automotive_design' ) ;
#7372=CARTESIAN_POINT ( 'NONE',  ( 0.000000000000000000, 3.306546357697853733E-16, -2.700000000000000178 ) ) ;
#7396=EDGE_CURVE ( 'NONE', #7275, #3159, #13656, .T. ) ;
#7483=CARTESIAN_POINT ( 'NONE',  ( 0.000000000000000000, 0.000000000000000000, 0.000000000000000000 ) ) ;
#7699=EDGE_CURVE ( 'NONE', #2880, #4156, #9560, .T. ) ;
#7736=ADVANCED_BREP_SHAPE_REPRESENTATION ( '', ( #2529, #9440 ), #13 ) ;
#7781=VECTOR ( 'NONE', #14059, 1000.000000000000000 ) ;
#7892=DIRECTION ( 'NONE',  ( 0.000000000000000000, 0.000000000000000000, -1.000000000000000000 ) ) ;
#7905=CYLINDRICAL_SURFACE ( 'NONE', #4680, 2.700000000000000178 ) ;
#7955=DIRECTION ( 'NONE',  ( 1.000000000000000000, 0.000000000000000000, 0.000000000000000000 ) ) ;
#8074=LINE ( 'NONE', #4392, #12914 ) ;
#8119=DIRECTION ( 'NONE',  ( 1.000000000000000000, 0.000000000000000000, 0.000000000000000000 ) ) ;
#8133=ADVANCED_FACE ( 'NONE', ( #4893, #9389 ), #8275, .F. ) ;
#8275=PLANE ( 'NONE',  #3560 ) ;
#8481=ADVANCED_FACE ( 'NONE', ( #10629 ), #1325, .F. ) ;
#8555=CARTESIAN_POINT ( 'NONE',  ( 1.600000000000000089, 0.000000000000000000, 0.000000000000000000 ) ) ;
#8562=EDGE_CURVE ( 'NONE', #13362, #1078, #961, .T. ) ;
#8708=PRODUCT_DEFINITION_CONTEXT ( 'detailed design', #7349, 'design' ) ;
#8761=VECTOR ( 'NONE', #8980, 1000.000000000000000 ) ;
#8980=DIRECTION ( 'NONE',  ( -1.000000000000000000, -0.000000000000000000, -0.000000000000000000 ) ) ;
#9235=DIRECTION ( 'NONE',  ( -1.000000000000000000, -0.000000000000000000, -0.000000000000000000 ) ) ;
#9265=SHAPE_REPRESENTATION_RELATIONSHIP ( 'NONE' , 'NONE' ,  #3392, #7736 ) ;
#9283=ORIENTED_EDGE ( 'NONE', *, *, #4940, .T. ) ;
#9297=PRODUCT_DEFINITION ( 'UNKNOWN', '', #6661, #8708 ) ;
#9389=FACE_BOUND ( 'NONE', #4813, .T. ) ;
#9440=AXIS2_PLACEMENT_3D ( 'NONE', #4347, #14302, #6417 ) ;
#9526=ORIENTED_EDGE ( 'NONE', *, *, #7699, .T. ) ;
#9558=SURFACE_STYLE_FILL_AREA ( #7189 ) ;
#9560=LINE ( 'NONE', #10733, #7781 ) ;
#9687=ORIENTED_EDGE ( 'NONE', *, *, #7396, .F. ) ;
#9752=UNCERTAINTY_MEASURE_WITH_UNIT (LENGTH_MEASURE( 1.000000000000000082E-05 ), #1212, 'distance_accuracy_value', 'NONE');
#10052=CARTESIAN_POINT ( 'NONE',  ( 1.600000000000000089, 3.306546357697853733E-16, -2.700000000000000178 ) ) ;
#10055=DIRECTION ( 'NONE',  ( 1.000000000000000000, 0.000000000000000000, 0.000000000000000000 ) ) ;
#10153=AXIS2_PLACEMENT_3D ( 'NONE', #7483, #10055, #11980 ) ;
#10191=ORIENTED_EDGE ( 'NONE', *, *, #392, .F. ) ;
#10196=( LENGTH_UNIT ( ) NAMED_UNIT ( * ) SI_UNIT ( .MILLI., .METRE. ) );
#10414=DIRECTION ( 'NONE',  ( 0.000000000000000000, 0.000000000000000000, 1.000000000000000000 ) ) ;
#10441=DIRECTION ( 'NONE',  ( 1.000000000000000000, 0.000000000000000000, 0.000000000000000000 ) ) ;
#10442=( NAMED_UNIT ( * ) SI_UNIT ( $, .STERADIAN. ) SOLID_ANGLE_UNIT ( ) );
#10462=EDGE_CURVE ( 'NONE', #2880, #238, #5455, .T. ) ;
#10487=DIRECTION ( 'NONE',  ( 0.000000000000000000, 0.000000000000000000, 1.000000000000000000 ) ) ;
#10559=DIRECTION ( 'NONE',  ( -1.000000000000000000, -0.000000000000000000, -0.000000000000000000 ) ) ;
#10581=FILL_AREA_STYLE_COLOUR ( '', #5932 ) ;
#10629=FACE_OUTER_BOUND ( 'NONE', #1973, .T. ) ;
#10733=CARTESIAN_POINT ( 'NONE',  ( 1.600000000000000089, 0.000000000000000000, 7.000000000000000000 ) ) ;
#10843=ORIENTED_EDGE ( 'NONE', *, *, #6815, .T. ) ;
#10907=EDGE_LOOP ( 'NONE', ( #1488, #5515, #10843, #4262 ) ) ;
#10935=ORIENTED_EDGE ( 'NONE', *, *, #5661, .T. ) ;
#11405=VERTEX_POINT ( 'NONE', #6226 ) ;
#11410=EDGE_CURVE ( 'NONE', #4156, #11405, #2887, .T. ) ;
#11419=DIRECTION ( 'NONE',  ( -1.000000000000000000, -0.000000000000000000, -0.000000000000000000 ) ) ;
#11536=CARTESIAN_POINT ( 'NONE',  ( 0.000000000000000000, 0.000000000000000000, 0.000000000000000000 ) ) ;
#11713=DIRECTION ( 'NONE',  ( 0.000000000000000000, 0.000000000000000000, 1.000000000000000000 ) ) ;
#11739=FACE_OUTER_BOUND ( 'NONE', #912, .T. ) ;
#11953=AXIS2_PLACEMENT_3D ( 'NONE', #8555, #8119, #13524 ) ;
#11980=DIRECTION ( 'NONE',  ( 0.000000000000000000, 0.000000000000000000, -1.000000000000000000 ) ) ;
#11981=ORIENTED_EDGE ( 'NONE', *, *, #6531, .T. ) ;
#12057=( GEOMETRIC_REPRESENTATION_CONTEXT ( 3 ) GLOBAL_UNCERTAINTY_ASSIGNED_CONTEXT ( ( #13885 ) ) GLOBAL_UNIT_ASSIGNED_CONTEXT ( ( #12645, #5941, #10442 ) ) REPRESENTATION_CONTEXT ( 'NONE', 'WORKASPACE' ) );
#12146=LINE ( 'NONE', #2030, #8761 ) ;
#12281=MECHANICAL_DESIGN_GEOMETRIC_PRESENTATION_REPRESENTATION('',(#6640),#12057);
#12458=SHAPE_DEFINITION_REPRESENTATION ( #3343, #3392 ) ;
#12645=( LENGTH_UNIT ( ) NAMED_UNIT ( * ) SI_UNIT ( .MILLI., .METRE. ) );
#12672=CIRCLE ( 'NONE', #4420, 2.700000000000000178 ) ;
#12805=( NAMED_UNIT ( * ) SI_UNIT ( $, .STERADIAN. ) SOLID_ANGLE_UNIT ( ) );
#12871=( NAMED_UNIT ( * ) PLANE_ANGLE_UNIT ( ) SI_UNIT ( $, .RADIAN. ) );
#12914=VECTOR ( 'NONE', #1210, 1000.000000000000000 ) ;
#13313=DIRECTION ( 'NONE',  ( 0.000000000000000000, 0.000000000000000000, -1.000000000000000000 ) ) ;
#13362=VERTEX_POINT ( 'NONE', #14050 ) ;
#13437=( NAMED_UNIT ( * ) SI_UNIT ( $, .STERADIAN. ) SOLID_ANGLE_UNIT ( ) );
#13524=DIRECTION ( 'NONE',  ( 0.000000000000000000, 0.000000000000000000, -1.000000000000000000 ) ) ;
#13581=FACE_OUTER_BOUND ( 'NONE', #10907, .T. ) ;
#13617=ORIENTED_EDGE ( 'NONE', *, *, #11410, .F. ) ;
#13656=CIRCLE ( 'NONE', #5408, 2.700000000000000178 ) ;
#13883=AXIS2_PLACEMENT_3D ( 'NONE', #6921, #11419, #5806 ) ;
#13885=UNCERTAINTY_MEASURE_WITH_UNIT (LENGTH_MEASURE( 1.000000000000000082E-05 ), #12645, 'distance_accuracy_value', 'NONE');
#13888=CYLINDRICAL_SURFACE ( 'NONE', #421, 7.000000000000000000 ) ;
#14002=CLOSED_SHELL ( 'NONE', ( #8481, #1788, #52, #8133, #3019, #2588 ) ) ;
#14050=CARTESIAN_POINT ( 'NONE',  ( 0.000000000000000000, 0.000000000000000000, 2.700000000000000178 ) ) ;
#14059=DIRECTION ( 'NONE',  ( -1.000000000000000000, -0.000000000000000000, -0.000000000000000000 ) ) ;
#14272=LINE ( 'NONE', #2831, #6343 ) ;
#14302=DIRECTION ( 'NONE',  ( 0.000000000000000000, 0.000000000000000000, 1.000000000000000000 ) ) ;
#14447=ORIENTED_EDGE ( 'NONE', *, *, #4923, .T. ) ;
#14542=( NAMED_UNIT ( * ) PLANE_ANGLE_UNIT ( ) SI_UNIT ( $, .RADIAN. ) );
#14675=COLOUR_RGB('Black',0.12,0.14,0.17);
#14676=FILL_AREA_STYLE_COLOUR('',#14675);
#14677=FILL_AREA_STYLE('',(#14676));
#14678=SURFACE_STYLE_FILL_AREA(#14677);
#14679=SURFACE_SIDE_STYLE('',(#14678));
#14680=SURFACE_STYLE_USAGE(.BOTH.,#14679);
#14681=PRESENTATION_STYLE_ASSIGNMENT((#14680));
ENDSEC;
END-ISO-10303-21;
